ISO-10303-21;
HEADER;
/* Generated by software containing ST-Developer
 * from STEP Tools, Inc. (www.steptools.com) 
 */

FILE_DESCRIPTION(
/* description */ ('Over-Centre Plunger Toggle Clamp on Slotted Fixture Frame'),
/* implementation_level */ '2;1');

FILE_NAME(
/* name */ 
'M4x10 Cap Screw.step',
/* time_stamp */ '2026-10-28T03:23:24-07:00',
/* author */ (''),
/* organization */ (''),
/* preprocessor_version */ 'ST-DEVELOPER v20.2',
/* originating_system */ 'Autodesk Translation Framework v15.17.0.0',
/* authorisation */ '');

FILE_SCHEMA (('AUTOMOTIVE_DESIGN { 1 0 10303 214 3 1 1 }'));
ENDSEC;

DATA;
#10=MECHANICAL_DESIGN_GEOMETRIC_PRESENTATION_REPRESENTATION('',(#554),#15212);
#399=ORIENTED_CLOSED_SHELL('',*,#8288,.F.);
#403=BREP_WITH_VOIDS('Body1',#8289,(#399));
#418=CONICAL_SURFACE('',#9528,0.325,0.785398163397448);
#419=CONICAL_SURFACE('',#9532,0.335,0.785398163397448);
#420=CONICAL_SURFACE('',#9536,0.21,0.463647609000806);
#462=SHAPE_REPRESENTATION_RELATIONSHIP('SRR','None',#15439,#504);
#504=ADVANCED_BREP_SHAPE_REPRESENTATION('',(#403),#15201);
#554=STYLED_ITEM('',(#15726),#403);
#766=FACE_BOUND('',#2135,.T.);
#1024=PLANE('',#9516);
#1025=PLANE('',#9517);
#1026=PLANE('',#9518);
#1027=PLANE('',#9519);
#1028=PLANE('',#9520);
#1029=PLANE('',#9521);
#1030=PLANE('',#9522);
#1031=PLANE('',#9523);
#1032=PLANE('',#9524);
#1033=PLANE('',#9526);
#1034=PLANE('',#9534);
#1480=FACE_OUTER_BOUND('',#2121,.T.);
#1481=FACE_OUTER_BOUND('',#2122,.T.);
#1482=FACE_OUTER_BOUND('',#2123,.T.);
#1483=FACE_OUTER_BOUND('',#2124,.T.);
#1484=FACE_OUTER_BOUND('',#2125,.T.);
#1485=FACE_OUTER_BOUND('',#2126,.T.);
#1486=FACE_OUTER_BOUND('',#2127,.T.);
#1487=FACE_OUTER_BOUND('',#2128,.T.);
#1488=FACE_OUTER_BOUND('',#2129,.T.);
#1489=FACE_OUTER_BOUND('',#2130,.T.);
#1490=FACE_OUTER_BOUND('',#2131,.T.);
#1491=FACE_OUTER_BOUND('',#2132,.T.);
#1492=FACE_OUTER_BOUND('',#2133,.T.);
#1493=FACE_OUTER_BOUND('',#2134,.T.);
#1494=FACE_OUTER_BOUND('',#2136,.T.);
#1495=FACE_OUTER_BOUND('',#2137,.T.);
#2121=EDGE_LOOP('',(#7253,#7254,#7255,#7256));
#2122=EDGE_LOOP('',(#7257,#7258,#7259,#7260));
#2123=EDGE_LOOP('',(#7261,#7262,#7263,#7264));
#2124=EDGE_LOOP('',(#7265,#7266,#7267,#7268));
#2125=EDGE_LOOP('',(#7269,#7270,#7271,#7272));
#2126=EDGE_LOOP('',(#7273,#7274,#7275,#7276));
#2127=EDGE_LOOP('',(#7277,#7278,#7279,#7280,#7281,#7282));
#2128=EDGE_LOOP('',(#7283,#7284,#7285,#7286,#7287,#7288));
#2129=EDGE_LOOP('',(#7289));
#2130=EDGE_LOOP('',(#7290));
#2131=EDGE_LOOP('',(#7291,#7292,#7293,#7294));
#2132=EDGE_LOOP('',(#7295,#7296,#7297,#7298));
#2133=EDGE_LOOP('',(#7299,#7300,#7301,#7302));
#2134=EDGE_LOOP('',(#7303));
#2135=EDGE_LOOP('',(#7304));
#2136=EDGE_LOOP('',(#7305,#7306,#7307,#7308));
#2137=EDGE_LOOP('',(#7309,#7310,#7311,#7312));
#2737=LINE('',#14616,#3367);
#2738=LINE('',#14618,#3368);
#2739=LINE('',#14620,#3369);
#2740=LINE('',#14621,#3370);
#2741=LINE('',#14624,#3371);
#2742=LINE('',#14626,#3372);
#2743=LINE('',#14627,#3373);
#2744=LINE('',#14630,#3374);
#2745=LINE('',#14632,#3375);
#2746=LINE('',#14633,#3376);
#2747=LINE('',#14636,#3377);
#2748=LINE('',#14638,#3378);
#2749=LINE('',#14639,#3379);
#2750=LINE('',#14642,#3380);
#2751=LINE('',#14644,#3381);
#2752=LINE('',#14645,#3382);
#2753=LINE('',#14647,#3383);
#2754=LINE('',#14648,#3384);
#2755=LINE('',#14660,#3385);
#2756=LINE('',#14664,#3386);
#2757=LINE('',#14668,#3387);
#2758=LINE('',#14675,#3388);
#2759=LINE('',#14677,#3389);
#3367=VECTOR('',#11768,1.);
#3368=VECTOR('',#11769,1.);
#3369=VECTOR('',#11770,1.);
#3370=VECTOR('',#11771,1.);
#3371=VECTOR('',#11774,1.);
#3372=VECTOR('',#11775,1.);
#3373=VECTOR('',#11776,1.);
#3374=VECTOR('',#11779,1.);
#3375=VECTOR('',#11780,1.);
#3376=VECTOR('',#11781,1.);
#3377=VECTOR('',#11784,1.);
#3378=VECTOR('',#11785,1.);
#3379=VECTOR('',#11786,1.);
#3380=VECTOR('',#11789,1.);
#3381=VECTOR('',#11790,1.);
#3382=VECTOR('',#11791,1.);
#3383=VECTOR('',#11794,1.);
#3384=VECTOR('',#11795,1.);
#3385=VECTOR('',#11812,0.325);
#3386=VECTOR('',#11817,0.35);
#3387=VECTOR('',#11822,0.335);
#3388=VECTOR('',#11831,0.21);
#3389=VECTOR('',#11834,0.2);
#3803=CIRCLE('',#9525,0.1954);
#3804=CIRCLE('',#9527,0.3);
#3805=CIRCLE('',#9529,0.35);
#3806=CIRCLE('',#9531,0.35);
#3807=CIRCLE('',#9533,0.32);
#3808=CIRCLE('',#9535,0.22);
#3809=CIRCLE('',#9537,0.1954);
#4427=VERTEX_POINT('',#14614);
#4428=VERTEX_POINT('',#14615);
#4429=VERTEX_POINT('',#14617);
#4430=VERTEX_POINT('',#14619);
#4431=VERTEX_POINT('',#14623);
#4432=VERTEX_POINT('',#14625);
#4433=VERTEX_POINT('',#14629);
#4434=VERTEX_POINT('',#14631);
#4435=VERTEX_POINT('',#14635);
#4436=VERTEX_POINT('',#14637);
#4437=VERTEX_POINT('',#14641);
#4438=VERTEX_POINT('',#14643);
#4439=VERTEX_POINT('',#14652);
#4440=VERTEX_POINT('',#14655);
#4441=VERTEX_POINT('',#14658);
#4442=VERTEX_POINT('',#14662);
#4443=VERTEX_POINT('',#14666);
#4444=VERTEX_POINT('',#14670);
#4445=VERTEX_POINT('',#14673);
#5387=EDGE_CURVE('',#4427,#4428,#2737,.T.);
#5388=EDGE_CURVE('',#4428,#4429,#2738,.T.);
#5389=EDGE_CURVE('',#4429,#4430,#2739,.T.);
#5390=EDGE_CURVE('',#4427,#4430,#2740,.T.);
#5391=EDGE_CURVE('',#4428,#4431,#2741,.T.);
#5392=EDGE_CURVE('',#4431,#4432,#2742,.T.);
#5393=EDGE_CURVE('',#4432,#4429,#2743,.T.);
#5394=EDGE_CURVE('',#4431,#4433,#2744,.T.);
#5395=EDGE_CURVE('',#4433,#4434,#2745,.T.);
#5396=EDGE_CURVE('',#4434,#4432,#2746,.T.);
#5397=EDGE_CURVE('',#4433,#4435,#2747,.T.);
#5398=EDGE_CURVE('',#4435,#4436,#2748,.T.);
#5399=EDGE_CURVE('',#4436,#4434,#2749,.T.);
#5400=EDGE_CURVE('',#4435,#4437,#2750,.T.);
#5401=EDGE_CURVE('',#4437,#4438,#2751,.T.);
#5402=EDGE_CURVE('',#4438,#4436,#2752,.T.);
#5403=EDGE_CURVE('',#4437,#4427,#2753,.T.);
#5404=EDGE_CURVE('',#4430,#4438,#2754,.T.);
#5405=EDGE_CURVE('',#4439,#4439,#3803,.T.);
#5406=EDGE_CURVE('',#4440,#4440,#3804,.T.);
#5407=EDGE_CURVE('',#4441,#4441,#3805,.T.);
#5408=EDGE_CURVE('',#4441,#4440,#2755,.T.);
#5409=EDGE_CURVE('',#4442,#4442,#3806,.T.);
#5410=EDGE_CURVE('',#4442,#4441,#2756,.T.);
#5411=EDGE_CURVE('',#4443,#4443,#3807,.T.);
#5412=EDGE_CURVE('',#4443,#4442,#2757,.T.);
#5413=EDGE_CURVE('',#4444,#4444,#3808,.T.);
#5414=EDGE_CURVE('',#4445,#4445,#3809,.F.);
#5415=EDGE_CURVE('',#4445,#4444,#2758,.T.);
#5416=EDGE_CURVE('',#4439,#4445,#2759,.T.);
#7253=ORIENTED_EDGE('',*,*,#5387,.T.);
#7254=ORIENTED_EDGE('',*,*,#5388,.T.);
#7255=ORIENTED_EDGE('',*,*,#5389,.T.);
#7256=ORIENTED_EDGE('',*,*,#5390,.F.);
#7257=ORIENTED_EDGE('',*,*,#5391,.T.);
#7258=ORIENTED_EDGE('',*,*,#5392,.T.);
#7259=ORIENTED_EDGE('',*,*,#5393,.T.);
#7260=ORIENTED_EDGE('',*,*,#5388,.F.);
#7261=ORIENTED_EDGE('',*,*,#5394,.T.);
#7262=ORIENTED_EDGE('',*,*,#5395,.T.);
#7263=ORIENTED_EDGE('',*,*,#5396,.T.);
#7264=ORIENTED_EDGE('',*,*,#5392,.F.);
#7265=ORIENTED_EDGE('',*,*,#5397,.T.);
#7266=ORIENTED_EDGE('',*,*,#5398,.T.);
#7267=ORIENTED_EDGE('',*,*,#5399,.T.);
#7268=ORIENTED_EDGE('',*,*,#5395,.F.);
#7269=ORIENTED_EDGE('',*,*,#5400,.T.);
#7270=ORIENTED_EDGE('',*,*,#5401,.T.);
#7271=ORIENTED_EDGE('',*,*,#5402,.T.);
#7272=ORIENTED_EDGE('',*,*,#5398,.F.);
#7273=ORIENTED_EDGE('',*,*,#5403,.T.);
#7274=ORIENTED_EDGE('',*,*,#5390,.T.);
#7275=ORIENTED_EDGE('',*,*,#5404,.T.);
#7276=ORIENTED_EDGE('',*,*,#5401,.F.);
#7277=ORIENTED_EDGE('',*,*,#5403,.F.);
#7278=ORIENTED_EDGE('',*,*,#5400,.F.);
#7279=ORIENTED_EDGE('',*,*,#5397,.F.);
#7280=ORIENTED_EDGE('',*,*,#5394,.F.);
#7281=ORIENTED_EDGE('',*,*,#5391,.F.);
#7282=ORIENTED_EDGE('',*,*,#5387,.F.);
#7283=ORIENTED_EDGE('',*,*,#5404,.F.);
#7284=ORIENTED_EDGE('',*,*,#5389,.F.);
#7285=ORIENTED_EDGE('',*,*,#5393,.F.);
#7286=ORIENTED_EDGE('',*,*,#5396,.F.);
#7287=ORIENTED_EDGE('',*,*,#5399,.F.);
#7288=ORIENTED_EDGE('',*,*,#5402,.F.);
#7289=ORIENTED_EDGE('',*,*,#5405,.F.);
#7290=ORIENTED_EDGE('',*,*,#5406,.F.);
#7291=ORIENTED_EDGE('',*,*,#5407,.F.);
#7292=ORIENTED_EDGE('',*,*,#5408,.T.);
#7293=ORIENTED_EDGE('',*,*,#5406,.T.);
#7294=ORIENTED_EDGE('',*,*,#5408,.F.);
#7295=ORIENTED_EDGE('',*,*,#5409,.F.);
#7296=ORIENTED_EDGE('',*,*,#5410,.T.);
#7297=ORIENTED_EDGE('',*,*,#5407,.T.);
#7298=ORIENTED_EDGE('',*,*,#5410,.F.);
#7299=ORIENTED_EDGE('',*,*,#5411,.F.);
#7300=ORIENTED_EDGE('',*,*,#5412,.T.);
#7301=ORIENTED_EDGE('',*,*,#5409,.T.);
#7302=ORIENTED_EDGE('',*,*,#5412,.F.);
#7303=ORIENTED_EDGE('',*,*,#5411,.T.);
#7304=ORIENTED_EDGE('',*,*,#5413,.F.);
#7305=ORIENTED_EDGE('',*,*,#5414,.F.);
#7306=ORIENTED_EDGE('',*,*,#5415,.T.);
#7307=ORIENTED_EDGE('',*,*,#5413,.T.);
#7308=ORIENTED_EDGE('',*,*,#5415,.F.);
#7309=ORIENTED_EDGE('',*,*,#5405,.T.);
#7310=ORIENTED_EDGE('',*,*,#5416,.T.);
#7311=ORIENTED_EDGE('',*,*,#5414,.T.);
#7312=ORIENTED_EDGE('',*,*,#5416,.F.);
#7738=CYLINDRICAL_SURFACE('',#9530,0.35);
#7739=CYLINDRICAL_SURFACE('',#9538,0.1954);
#8152=ADVANCED_FACE('',(#1480),#1024,.F.);
#8153=ADVANCED_FACE('',(#1481),#1025,.F.);
#8154=ADVANCED_FACE('',(#1482),#1026,.F.);
#8155=ADVANCED_FACE('',(#1483),#1027,.F.);
#8156=ADVANCED_FACE('',(#1484),#1028,.F.);
#8157=ADVANCED_FACE('',(#1485),#1029,.F.);
#8158=ADVANCED_FACE('',(#1486),#1030,.F.);
#8159=ADVANCED_FACE('',(#1487),#1031,.F.);
#8160=ADVANCED_FACE('',(#1488),#1032,.F.);
#8161=ADVANCED_FACE('',(#1489),#1033,.T.);
#8162=ADVANCED_FACE('',(#1490),#418,.T.);
#8163=ADVANCED_FACE('',(#1491),#7738,.T.);
#8164=ADVANCED_FACE('',(#1492),#419,.T.);
#8165=ADVANCED_FACE('',(#1493,#766),#1034,.T.);
#8166=ADVANCED_FACE('',(#1494),#420,.T.);
#8167=ADVANCED_FACE('',(#1495),#7739,.T.);
#8288=CLOSED_SHELL('',(#8152,#8153,#8154,#8155,#8156,#8157,#8158,#8159));
#8289=CLOSED_SHELL('',(#8160,#8161,#8162,#8163,#8164,#8165,#8166,#8167));
#9515=AXIS2_PLACEMENT_3D('',#14612,#11764,#11765);
#9516=AXIS2_PLACEMENT_3D('',#14613,#11766,#11767);
#9517=AXIS2_PLACEMENT_3D('',#14622,#11772,#11773);
#9518=AXIS2_PLACEMENT_3D('',#14628,#11777,#11778);
#9519=AXIS2_PLACEMENT_3D('',#14634,#11782,#11783);
#9520=AXIS2_PLACEMENT_3D('',#14640,#11787,#11788);
#9521=AXIS2_PLACEMENT_3D('',#14646,#11792,#11793);
#9522=AXIS2_PLACEMENT_3D('',#14649,#11796,#11797);
#9523=AXIS2_PLACEMENT_3D('',#14650,#11798,#11799);
#9524=AXIS2_PLACEMENT_3D('',#14651,#11800,#11801);
#9525=AXIS2_PLACEMENT_3D('',#14653,#11802,#11803);
#9526=AXIS2_PLACEMENT_3D('',#14654,#11804,#11805);
#9527=AXIS2_PLACEMENT_3D('',#14656,#11806,#11807);
#9528=AXIS2_PLACEMENT_3D('',#14657,#11808,#11809);
#9529=AXIS2_PLACEMENT_3D('',#14659,#11810,#11811);
#9530=AXIS2_PLACEMENT_3D('',#14661,#11813,#11814);
#9531=AXIS2_PLACEMENT_3D('',#14663,#11815,#11816);
#9532=AXIS2_PLACEMENT_3D('',#14665,#11818,#11819);
#9533=AXIS2_PLACEMENT_3D('',#14667,#11820,#11821);
#9534=AXIS2_PLACEMENT_3D('',#14669,#11823,#11824);
#9535=AXIS2_PLACEMENT_3D('',#14671,#11825,#11826);
#9536=AXIS2_PLACEMENT_3D('',#14672,#11827,#11828);
#9537=AXIS2_PLACEMENT_3D('',#14674,#11829,#11830);
#9538=AXIS2_PLACEMENT_3D('',#14676,#11832,#11833);
#11764=DIRECTION('axis',(0.,0.,1.));
#11765=DIRECTION('refdir',(1.,0.,0.));
#11766=DIRECTION('center_axis',(0.866025403784439,0.,-0.5));
#11767=DIRECTION('ref_axis',(0.5,0.,0.866025403784439));
#11768=DIRECTION('',(-0.5,0.,-0.866025403784439));
#11769=DIRECTION('',(0.,-1.,0.));
#11770=DIRECTION('',(0.5,0.,0.866025403784439));
#11771=DIRECTION('',(0.,-1.,0.));
#11772=DIRECTION('center_axis',(1.60246890531964E-16,0.,-1.));
#11773=DIRECTION('ref_axis',(1.,0.,1.60246890531964E-16));
#11774=DIRECTION('',(-1.,0.,-1.60246890531964E-16));
#11775=DIRECTION('',(0.,-1.,0.));
#11776=DIRECTION('',(1.,0.,1.60246890531964E-16));
#11777=DIRECTION('center_axis',(-0.866025403784439,0.,-0.5));
#11778=DIRECTION('ref_axis',(0.5,0.,-0.866025403784439));
#11779=DIRECTION('',(-0.5,0.,0.866025403784439));
#11780=DIRECTION('',(0.,-1.,0.));
#11781=DIRECTION('',(0.5,0.,-0.866025403784439));
#11782=DIRECTION('center_axis',(-0.866025403784439,0.,0.5));
#11783=DIRECTION('ref_axis',(-0.5,0.,-0.866025403784439));
#11784=DIRECTION('',(0.5,0.,0.866025403784439));
#11785=DIRECTION('',(0.,-1.,0.));
#11786=DIRECTION('',(-0.5,0.,-0.866025403784439));
#11787=DIRECTION('center_axis',(-1.60246890531964E-16,0.,1.));
#11788=DIRECTION('ref_axis',(-1.,0.,-1.60246890531964E-16));
#11789=DIRECTION('',(1.,0.,1.60246890531964E-16));
#11790=DIRECTION('',(0.,-1.,0.));
#11791=DIRECTION('',(-1.,0.,-1.60246890531964E-16));
#11792=DIRECTION('center_axis',(0.866025403784439,0.,0.5));
#11793=DIRECTION('ref_axis',(-0.5,0.,0.866025403784439));
#11794=DIRECTION('',(0.5,0.,-0.866025403784439));
#11795=DIRECTION('',(-0.5,0.,0.866025403784439));
#11796=DIRECTION('center_axis',(0.,1.,0.));
#11797=DIRECTION('ref_axis',(1.,0.,0.));
#11798=DIRECTION('center_axis',(0.,-1.,0.));
#11799=DIRECTION('ref_axis',(0.,0.,-1.));
#11800=DIRECTION('center_axis',(0.,1.,0.));
#11801=DIRECTION('ref_axis',(1.,0.,0.));
#11802=DIRECTION('center_axis',(0.,1.,0.));
#11803=DIRECTION('ref_axis',(1.,0.,0.));
#11804=DIRECTION('center_axis',(0.,1.,0.));
#11805=DIRECTION('ref_axis',(0.,0.,1.));
#11806=DIRECTION('center_axis',(0.,-1.,0.));
#11807=DIRECTION('ref_axis',(1.,0.,0.));
#11808=DIRECTION('center_axis',(0.,-1.,0.));
#11809=DIRECTION('ref_axis',(1.,0.,0.));
#11810=DIRECTION('center_axis',(0.,-1.,0.));
#11811=DIRECTION('ref_axis',(1.,0.,0.));
#11812=DIRECTION('',(0.707106781186547,0.707106781186548,8.65956056235493E-17));
#11813=DIRECTION('center_axis',(0.,-1.,0.));
#11814=DIRECTION('ref_axis',(1.,0.,0.));
#11815=DIRECTION('center_axis',(0.,-1.,0.));
#11816=DIRECTION('ref_axis',(1.,0.,0.));
#11817=DIRECTION('',(0.,1.,0.));
#11818=DIRECTION('center_axis',(0.,1.,0.));
#11819=DIRECTION('ref_axis',(1.,0.,0.));
#11820=DIRECTION('center_axis',(0.,-1.,0.));
#11821=DIRECTION('ref_axis',(1.,0.,0.));
#11822=DIRECTION('',(-0.707106781186547,0.707106781186548,-8.65956056235493E-17));
#11823=DIRECTION('center_axis',(0.,-1.,0.));
#11824=DIRECTION('ref_axis',(0.,0.,-1.));
#11825=DIRECTION('center_axis',(0.,-1.,0.));
#11826=DIRECTION('ref_axis',(1.,0.,0.));
#11827=DIRECTION('center_axis',(0.,1.,0.));
#11828=DIRECTION('ref_axis',(1.,0.,0.));
#11829=DIRECTION('center_axis',(0.,1.,0.));
#11830=DIRECTION('ref_axis',(1.,0.,0.));
#11831=DIRECTION('',(-0.447213595499958,0.894427190999916,-5.47678698264203E-17));
#11832=DIRECTION('center_axis',(0.,-1.,0.));
#11833=DIRECTION('ref_axis',(1.,0.,0.));
#11834=DIRECTION('',(0.,1.,0.));
#14612=CARTESIAN_POINT('',(0.,0.,0.));
#14613=CARTESIAN_POINT('Origin',(0.0866025403784439,-0.4,-0.15));
#14614=CARTESIAN_POINT('',(0.173205080756888,-0.4,0.));
#14615=CARTESIAN_POINT('',(0.0866025403784439,-0.4,-0.15));
#14616=CARTESIAN_POINT('',(0.173205080756888,-0.4,0.));
#14617=CARTESIAN_POINT('',(0.0866025403784439,-0.64,-0.15));
#14618=CARTESIAN_POINT('',(0.0866025403784439,-0.4,-0.15));
#14619=CARTESIAN_POINT('',(0.173205080756888,-0.64,0.));
#14620=CARTESIAN_POINT('',(0.173205080756888,-0.64,0.));
#14621=CARTESIAN_POINT('',(0.173205080756888,-0.4,0.));
#14622=CARTESIAN_POINT('Origin',(-0.0866025403784438,-0.4,-0.15));
#14623=CARTESIAN_POINT('',(-0.0866025403784438,-0.4,-0.15));
#14624=CARTESIAN_POINT('',(0.0866025403784439,-0.4,-0.15));
#14625=CARTESIAN_POINT('',(-0.0866025403784438,-0.64,-0.15));
#14626=CARTESIAN_POINT('',(-0.0866025403784438,-0.4,-0.15));
#14627=CARTESIAN_POINT('',(0.0866025403784439,-0.64,-0.15));
#14628=CARTESIAN_POINT('Origin',(-0.173205080756888,-0.4,-2.77555756156289E-17));
#14629=CARTESIAN_POINT('',(-0.173205080756888,-0.4,-2.12115047744981E-17));
#14630=CARTESIAN_POINT('',(-0.0866025403784438,-0.4,-0.15));
#14631=CARTESIAN_POINT('',(-0.173205080756888,-0.64,-2.77555756156289E-17));
#14632=CARTESIAN_POINT('',(-0.173205080756888,-0.4,-2.12115047744981E-17));
#14633=CARTESIAN_POINT('',(-0.0866025403784438,-0.64,-0.15));
#14634=CARTESIAN_POINT('Origin',(-0.0866025403784439,-0.4,0.15));
#14635=CARTESIAN_POINT('',(-0.0866025403784439,-0.4,0.15));
#14636=CARTESIAN_POINT('',(-0.173205080756888,-0.4,-2.12115047744981E-17));
#14637=CARTESIAN_POINT('',(-0.0866025403784439,-0.64,0.15));
#14638=CARTESIAN_POINT('',(-0.0866025403784439,-0.4,0.15));
#14639=CARTESIAN_POINT('',(-0.173205080756888,-0.64,-2.12115047744981E-17));
#14640=CARTESIAN_POINT('Origin',(0.0866025403784439,-0.4,0.15));
#14641=CARTESIAN_POINT('',(0.0866025403784439,-0.4,0.15));
#14642=CARTESIAN_POINT('',(-0.0866025403784439,-0.4,0.15));
#14643=CARTESIAN_POINT('',(0.0866025403784439,-0.64,0.15));
#14644=CARTESIAN_POINT('',(0.0866025403784439,-0.4,0.15));
#14645=CARTESIAN_POINT('',(-0.0866025403784439,-0.64,0.15));
#14646=CARTESIAN_POINT('Origin',(0.173205080756888,-0.4,0.));
#14647=CARTESIAN_POINT('',(0.0866025403784439,-0.4,0.15));
#14648=CARTESIAN_POINT('',(0.0866025403784439,-0.64,0.15));
#14649=CARTESIAN_POINT('Origin',(0.,-0.4,-2.77555756156289E-17));
#14650=CARTESIAN_POINT('Origin',(0.,-0.64,-2.77555756156289E-17));
#14651=CARTESIAN_POINT('Origin',(0.,-1.,0.));
#14652=CARTESIAN_POINT('',(-0.1954,-1.,2.39295984553393E-17));
#14653=CARTESIAN_POINT('Origin',(0.,-1.,0.));
#14654=CARTESIAN_POINT('Origin',(0.3,0.4,0.));
#14655=CARTESIAN_POINT('',(-0.3,0.4,-3.67394039744206E-17));
#14656=CARTESIAN_POINT('Origin',(0.,0.4,0.));
#14657=CARTESIAN_POINT('Origin',(0.,0.375,0.));
#14658=CARTESIAN_POINT('',(-0.35,0.35,-4.28626379701573E-17));
#14659=CARTESIAN_POINT('Origin',(0.,0.35,0.));
#14660=CARTESIAN_POINT('',(-0.325,0.375,-3.9801020972289E-17));
#14661=CARTESIAN_POINT('Origin',(0.,0.19,0.));
#14662=CARTESIAN_POINT('',(-0.35,0.03,-4.28626379701574E-17));
#14663=CARTESIAN_POINT('Origin',(0.,0.03,0.));
#14664=CARTESIAN_POINT('',(-0.35,0.19,-4.28626379701574E-17));
#14665=CARTESIAN_POINT('Origin',(0.,0.0149999999999999,0.));
#14666=CARTESIAN_POINT('',(-0.32,-3.29597460435593E-17,-3.91886975727153E-17));
#14667=CARTESIAN_POINT('Origin',(0.,0.,0.));
#14668=CARTESIAN_POINT('',(-0.335,0.0149999999999999,-4.10256677714363E-17));
#14669=CARTESIAN_POINT('Origin',(0.22,0.,0.));
#14670=CARTESIAN_POINT('',(-0.22,-6.93889390390723E-18,-2.69422295812418E-17));
#14671=CARTESIAN_POINT('Origin',(0.,0.,0.));
#14672=CARTESIAN_POINT('Origin',(0.,-0.02,0.));
#14673=CARTESIAN_POINT('',(-0.1954,-0.0492,2.39295984553393E-17));
#14674=CARTESIAN_POINT('Origin',(0.,-0.0492,0.));
#14675=CARTESIAN_POINT('',(-0.21,-0.02,-2.57175827820944E-17));
#14676=CARTESIAN_POINT('Origin',(0.,-0.8,0.));
#14677=CARTESIAN_POINT('',(-0.1954,-0.8,-2.39295984553393E-17));
#15151=UNCERTAINTY_MEASURE_WITH_UNIT(LENGTH_MEASURE(0.001),#15213,
'DISTANCE_ACCURACY_VALUE',
'Maximum model space distance between geometric entities at asserted c
onnectivities');
#15162=UNCERTAINTY_MEASURE_WITH_UNIT(LENGTH_MEASURE(0.001),#15213,
'DISTANCE_ACCURACY_VALUE',
'Maximum model space distance between geometric entities at asserted c
onnectivities');
#15201=(
GEOMETRIC_REPRESENTATION_CONTEXT(3)
GLOBAL_UNCERTAINTY_ASSIGNED_CONTEXT((#15151))
GLOBAL_UNIT_ASSIGNED_CONTEXT((#15213,#15215,#15216))
REPRESENTATION_CONTEXT('','3D')
);
#15212=(
GEOMETRIC_REPRESENTATION_CONTEXT(3)
GLOBAL_UNCERTAINTY_ASSIGNED_CONTEXT((#15162))
GLOBAL_UNIT_ASSIGNED_CONTEXT((#15213,#15215,#15216))
REPRESENTATION_CONTEXT('','3D')
);
#15213=(
LENGTH_UNIT()
NAMED_UNIT(*)
SI_UNIT(.CENTI.,.METRE.)
);
#15215=(
NAMED_UNIT(*)
PLANE_ANGLE_UNIT()
SI_UNIT($,.RADIAN.)
);
#15216=(
NAMED_UNIT(*)
SI_UNIT($,.STERADIAN.)
SOLID_ANGLE_UNIT()
);
#15255=SHAPE_DEFINITION_REPRESENTATION(#15311,#15439);
#15311=PRODUCT_DEFINITION_SHAPE('',$,#15489);
#15439=SHAPE_REPRESENTATION('',(#9515),#15201);
#15450=PRODUCT_DEFINITION_CONTEXT('part definition',#15599,'design');
#15489=PRODUCT_DEFINITION('M4x10 Cap Screw','M4x10 Cap Screw',#15538,#15450);
#15538=PRODUCT_DEFINITION_FORMATION('',$,#15639);
#15599=APPLICATION_CONTEXT(
'Core Data for Automotive Mechanical Design Process');
#15600=PRODUCT_CONTEXT('part definition',#15599,'mechanical');
#15639=PRODUCT('M4x10 Cap Screw','M4x10 Cap Screw','M4x10 Cap Screw',(#15600));
#15720=COLOUR_RGB('Black',0.12,0.14,0.17);
#15721=FILL_AREA_STYLE_COLOUR('',#15720);
#15722=FILL_AREA_STYLE('',(#15721));
#15723=SURFACE_STYLE_FILL_AREA(#15722);
#15724=SURFACE_SIDE_STYLE('',(#15723));
#15725=SURFACE_STYLE_USAGE(.BOTH.,#15724);
#15726=PRESENTATION_STYLE_ASSIGNMENT((#15725));
ENDSEC;
END-ISO-10303-21;
